ISO-10303-21;
HEADER;
FILE_DESCRIPTION((''),'2;1');
FILE_NAME('Bearing_Lock_Nut.step','2026-10-09T10:54:55-07:00',(''),(''),'','','');
FILE_SCHEMA (('AUTOMOTIVE_DESIGN { 1 0 10303 214 3 1 1 }'));
ENDSEC;
DATA;
#10=MECHANICAL_DESIGN_GEOMETRIC_PRESENTATION_REPRESENTATION('',(#605),#63824);
#83=(
BOUNDED_CURVE()
B_SPLINE_CURVE(2,(#53752,#53753,#53754),.UNSPECIFIED.,.F.,.F.)
B_SPLINE_CURVE_WITH_KNOTS((3,3),(0.,0.567460423251311),.UNSPECIFIED.)
CURVE()
GEOMETRIC_REPRESENTATION_ITEM()
RATIONAL_B_SPLINE_CURVE((1.,1.00278960134448,1.))
REPRESENTATION_ITEM('')
) ;
#84=(
BOUNDED_CURVE()
B_SPLINE_CURVE(2,(#53763,#53764,#53765),.UNSPECIFIED.,.F.,.F.)
B_SPLINE_CURVE_WITH_KNOTS((3,3),(0.,0.567460423251311),.UNSPECIFIED.)
CURVE()
GEOMETRIC_REPRESENTATION_ITEM()
RATIONAL_B_SPLINE_CURVE((1.,1.00278960136551,1.))
REPRESENTATION_ITEM('')
) ;
#85=(
BOUNDED_CURVE()
B_SPLINE_CURVE(2,(#53809,#53810,#53811),.UNSPECIFIED.,.F.,.F.)
B_SPLINE_CURVE_WITH_KNOTS((3,3),(0.,0.567460423251311),.UNSPECIFIED.)
CURVE()
GEOMETRIC_REPRESENTATION_ITEM()
RATIONAL_B_SPLINE_CURVE((1.,1.00278960136494,1.))
REPRESENTATION_ITEM('')
) ;
#86=(
BOUNDED_CURVE()
B_SPLINE_CURVE(2,(#53815,#53816,#53817),.UNSPECIFIED.,.F.,.F.)
B_SPLINE_CURVE_WITH_KNOTS((3,3),(0.,0.567460423251311),.UNSPECIFIED.)
CURVE()
GEOMETRIC_REPRESENTATION_ITEM()
RATIONAL_B_SPLINE_CURVE((1.,1.0027896013635,1.))
REPRESENTATION_ITEM('')
) ;
#87=(
BOUNDED_CURVE()
B_SPLINE_CURVE(2,(#53831,#53832,#53833),.UNSPECIFIED.,.F.,.F.)
B_SPLINE_CURVE_WITH_KNOTS((3,3),(0.,0.567460423251311),.UNSPECIFIED.)
CURVE()
GEOMETRIC_REPRESENTATION_ITEM()
RATIONAL_B_SPLINE_CURVE((1.,1.0027896013647,1.))
REPRESENTATION_ITEM('')
) ;
#88=(
BOUNDED_CURVE()
B_SPLINE_CURVE(2,(#53837,#53838,#53839),.UNSPECIFIED.,.F.,.F.)
B_SPLINE_CURVE_WITH_KNOTS((3,3),(0.,0.567460423251311),.UNSPECIFIED.)
CURVE()
GEOMETRIC_REPRESENTATION_ITEM()
RATIONAL_B_SPLINE_CURVE((1.,1.002789601364,1.))
REPRESENTATION_ITEM('')
) ;
#89=(
BOUNDED_CURVE()
B_SPLINE_CURVE(2,(#53853,#53854,#53855),.UNSPECIFIED.,.F.,.F.)
B_SPLINE_CURVE_WITH_KNOTS((3,3),(0.,0.56746042325131),.UNSPECIFIED.)
CURVE()
GEOMETRIC_REPRESENTATION_ITEM()
RATIONAL_B_SPLINE_CURVE((1.,1.00278960137803,1.))
REPRESENTATION_ITEM('')
) ;
#90=(
BOUNDED_CURVE()
B_SPLINE_CURVE(2,(#53859,#53860,#53861),.UNSPECIFIED.,.F.,.F.)
B_SPLINE_CURVE_WITH_KNOTS((3,3),(0.,0.56746042325131),.UNSPECIFIED.)
CURVE()
GEOMETRIC_REPRESENTATION_ITEM()
RATIONAL_B_SPLINE_CURVE((1.,1.00278960137803,1.))
REPRESENTATION_ITEM('')
) ;
#575=SHAPE_REPRESENTATION_RELATIONSHIP('SRR','None',#63889,#590) ;
#590=ADVANCED_BREP_SHAPE_REPRESENTATION('',(#620),#63819) ;
#605=STYLED_ITEM('',(#63966),#620) ;
#620=MANIFOLD_SOLID_BREP('Body1',#15504) ;
#757=FACE_BOUND('',#3216,.T.) ;
#758=FACE_BOUND('',#3235,.T.) ;
#1038=PLANE('',#17227) ;
#1039=PLANE('',#17228) ;
#1040=PLANE('',#17232) ;
#1041=PLANE('',#17245) ;
#1042=PLANE('',#17246) ;
#1043=PLANE('',#17253) ;
#1044=PLANE('',#17254) ;
#1045=PLANE('',#17261) ;
#1046=PLANE('',#17262) ;
#1047=PLANE('',#17269) ;
#1510=CYLINDRICAL_SURFACE('',#17229,25.) ;
#1511=CYLINDRICAL_SURFACE('',#17241,29.) ;
#1512=CYLINDRICAL_SURFACE('',#17247,25.) ;
#1513=CYLINDRICAL_SURFACE('',#17249,29.) ;
#1514=CYLINDRICAL_SURFACE('',#17255,25.) ;
#1515=CYLINDRICAL_SURFACE('',#17257,29.) ;
#1516=CYLINDRICAL_SURFACE('',#17263,25.) ;
#1517=CYLINDRICAL_SURFACE('',#17268,29.) ;
#1518=CYLINDRICAL_SURFACE('',#17271,18.7631) ;
#2219=FACE_OUTER_BOUND('',#3212,.T.) ;
#2220=FACE_OUTER_BOUND('',#3213,.T.) ;
#2221=FACE_OUTER_BOUND('',#3214,.T.) ;
#2222=FACE_OUTER_BOUND('',#3215,.T.) ;
#2223=FACE_OUTER_BOUND('',#3217,.T.) ;
#2224=FACE_OUTER_BOUND('',#3218,.T.) ;
#2225=FACE_OUTER_BOUND('',#3219,.T.) ;
#2226=FACE_OUTER_BOUND('',#3220,.T.) ;
#2227=FACE_OUTER_BOUND('',#3221,.T.) ;
#2228=FACE_OUTER_BOUND('',#3222,.T.) ;
#2229=FACE_OUTER_BOUND('',#3223,.T.) ;
#2230=FACE_OUTER_BOUND('',#3224,.T.) ;
#2231=FACE_OUTER_BOUND('',#3225,.T.) ;
#2232=FACE_OUTER_BOUND('',#3226,.T.) ;
#2233=FACE_OUTER_BOUND('',#3227,.T.) ;
#2234=FACE_OUTER_BOUND('',#3228,.T.) ;
#2235=FACE_OUTER_BOUND('',#3229,.T.) ;
#2236=FACE_OUTER_BOUND('',#3230,.T.) ;
#2237=FACE_OUTER_BOUND('',#3231,.T.) ;
#2238=FACE_OUTER_BOUND('',#3232,.T.) ;
#2239=FACE_OUTER_BOUND('',#3233,.T.) ;
#2240=FACE_OUTER_BOUND('',#3234,.T.) ;
#2241=FACE_OUTER_BOUND('',#3236,.T.) ;
#3212=EDGE_LOOP('',(#12848,#12849,#12850,#12851)) ;
#3213=EDGE_LOOP('',(#12852,#12853,#12854,#12855)) ;
#3214=EDGE_LOOP('',(#12856,#12857,#12858,#12859)) ;
#3215=EDGE_LOOP('',(#12860,#12861,#12862,#12863,#12864,#12865,#12866,#12867,
#12868,#12869,#12870,#12871,#12872,#12873,#12874,#12875)) ;
#3216=EDGE_LOOP('',(#12876)) ;
#3217=EDGE_LOOP('',(#12877,#12878,#12879,#12880)) ;
#3218=EDGE_LOOP('',(#12881,#12882,#12883,#12884)) ;
#3219=EDGE_LOOP('',(#12885,#12886,#12887,#12888)) ;
#3220=EDGE_LOOP('',(#12889,#12890,#12891,#12892)) ;
#3221=EDGE_LOOP('',(#12893,#12894,#12895,#12896)) ;
#3222=EDGE_LOOP('',(#12897,#12898,#12899,#12900)) ;
#3223=EDGE_LOOP('',(#12901,#12902,#12903,#12904)) ;
#3224=EDGE_LOOP('',(#12905,#12906,#12907,#12908)) ;
#3225=EDGE_LOOP('',(#12909,#12910,#12911,#12912)) ;
#3226=EDGE_LOOP('',(#12913,#12914,#12915,#12916)) ;
#3227=EDGE_LOOP('',(#12917,#12918,#12919,#12920)) ;
#3228=EDGE_LOOP('',(#12921,#12922,#12923,#12924)) ;
#3229=EDGE_LOOP('',(#12925,#12926,#12927,#12928)) ;
#3230=EDGE_LOOP('',(#12929,#12930,#12931,#12932)) ;
#3231=EDGE_LOOP('',(#12933,#12934,#12935,#12936)) ;
#3232=EDGE_LOOP('',(#12937,#12938,#12939,#12940)) ;
#3233=EDGE_LOOP('',(#12941,#12942,#12943,#12944)) ;
#3234=EDGE_LOOP('',(#12945,#12946,#12947,#12948,#12949,#12950,#12951,#12952)) ;
#3235=EDGE_LOOP('',(#12953)) ;
#3236=EDGE_LOOP('',(#12954,#12955,#12956,#12957)) ;
#4339=CIRCLE('',#17230,25.) ;
#4340=CIRCLE('',#17231,25.) ;
#4341=CIRCLE('',#17233,29.) ;
#4342=CIRCLE('',#17234,25.) ;
#4343=CIRCLE('',#17235,29.) ;
#4344=CIRCLE('',#17236,25.) ;
#4345=CIRCLE('',#17237,29.) ;
#4346=CIRCLE('',#17238,25.) ;
#4347=CIRCLE('',#17239,29.) ;
#4348=CIRCLE('',#17240,18.7631) ;
#4349=CIRCLE('',#17242,29.) ;
#4350=CIRCLE('',#17244,25.) ;
#4351=CIRCLE('',#17248,25.) ;
#4352=CIRCLE('',#17250,29.) ;
#4353=CIRCLE('',#17252,25.) ;
#4354=CIRCLE('',#17256,25.) ;
#4355=CIRCLE('',#17258,29.) ;
#4356=CIRCLE('',#17260,25.) ;
#4357=CIRCLE('',#17264,25.) ;
#4358=CIRCLE('',#17266,29.) ;
#4359=CIRCLE('',#17267,25.) ;
#4360=CIRCLE('',#17270,18.7631) ;
#5229=LINE('',#53756,#5885) ;
#5230=LINE('',#53758,#5886) ;
#5231=LINE('',#53759,#5887) ;
#5232=LINE('',#53767,#5888) ;
#5233=LINE('',#53769,#5889) ;
#5234=LINE('',#53770,#5890) ;
#5235=LINE('',#53778,#5891) ;
#5236=LINE('',#53782,#5892) ;
#5237=LINE('',#53786,#5893) ;
#5238=LINE('',#53790,#5894) ;
#5239=LINE('',#53794,#5895) ;
#5240=LINE('',#53798,#5896) ;
#5241=LINE('',#53805,#5897) ;
#5242=LINE('',#53818,#5898) ;
#5243=LINE('',#53819,#5899) ;
#5244=LINE('',#53821,#5900) ;
#5245=LINE('',#53827,#5901) ;
#5246=LINE('',#53840,#5902) ;
#5247=LINE('',#53841,#5903) ;
#5248=LINE('',#53843,#5904) ;
#5249=LINE('',#53849,#5905) ;
#5250=LINE('',#53862,#5906) ;
#5251=LINE('',#53863,#5907) ;
#5252=LINE('',#53865,#5908) ;
#5253=LINE('',#53876,#5909) ;
#5885=VECTOR('',#21547,10.) ;
#5886=VECTOR('',#21548,10.) ;
#5887=VECTOR('',#21549,10.) ;
#5888=VECTOR('',#21552,10.) ;
#5889=VECTOR('',#21553,10.) ;
#5890=VECTOR('',#21554,10.) ;
#5891=VECTOR('',#21565,10.) ;
#5892=VECTOR('',#21568,10.) ;
#5893=VECTOR('',#21571,10.) ;
#5894=VECTOR('',#21574,10.) ;
#5895=VECTOR('',#21577,10.) ;
#5896=VECTOR('',#21580,10.) ;
#5897=VECTOR('',#21589,10.) ;
#5898=VECTOR('',#21596,10.) ;
#5899=VECTOR('',#21597,10.) ;
#5900=VECTOR('',#21600,10.) ;
#5901=VECTOR('',#21609,10.) ;
#5902=VECTOR('',#21616,10.) ;
#5903=VECTOR('',#21617,10.) ;
#5904=VECTOR('',#21620,10.) ;
#5905=VECTOR('',#21629,10.) ;
#5906=VECTOR('',#21636,10.) ;
#5907=VECTOR('',#21637,10.) ;
#5908=VECTOR('',#21640,10.) ;
#5909=VECTOR('',#21659,18.7631) ;
#6951=VERTEX_POINT('',#53750) ;
#6952=VERTEX_POINT('',#53751) ;
#6953=VERTEX_POINT('',#53755) ;
#6954=VERTEX_POINT('',#53757) ;
#6955=VERTEX_POINT('',#53761) ;
#6956=VERTEX_POINT('',#53762) ;
#6957=VERTEX_POINT('',#53766) ;
#6958=VERTEX_POINT('',#53768) ;
#6959=VERTEX_POINT('',#53775) ;
#6960=VERTEX_POINT('',#53777) ;
#6961=VERTEX_POINT('',#53779) ;
#6962=VERTEX_POINT('',#53781) ;
#6963=VERTEX_POINT('',#53783) ;
#6964=VERTEX_POINT('',#53785) ;
#6965=VERTEX_POINT('',#53787) ;
#6966=VERTEX_POINT('',#53789) ;
#6967=VERTEX_POINT('',#53791) ;
#6968=VERTEX_POINT('',#53793) ;
#6969=VERTEX_POINT('',#53795) ;
#6970=VERTEX_POINT('',#53797) ;
#6971=VERTEX_POINT('',#53800) ;
#6972=VERTEX_POINT('',#53803) ;
#6973=VERTEX_POINT('',#53807) ;
#6974=VERTEX_POINT('',#53813) ;
#6975=VERTEX_POINT('',#53814) ;
#6976=VERTEX_POINT('',#53825) ;
#6977=VERTEX_POINT('',#53829) ;
#6978=VERTEX_POINT('',#53835) ;
#6979=VERTEX_POINT('',#53836) ;
#6980=VERTEX_POINT('',#53847) ;
#6981=VERTEX_POINT('',#53851) ;
#6982=VERTEX_POINT('',#53857) ;
#6983=VERTEX_POINT('',#53858) ;
#6984=VERTEX_POINT('',#53873) ;
#8978=EDGE_CURVE('',#6951,#6952,#83,.T.) ;
#8979=EDGE_CURVE('',#6953,#6951,#5229,.T.) ;
#8980=EDGE_CURVE('',#6954,#6953,#5230,.T.) ;
#8981=EDGE_CURVE('',#6952,#6954,#5231,.T.) ;
#8982=EDGE_CURVE('',#6955,#6956,#84,.T.) ;
#8983=EDGE_CURVE('',#6955,#6957,#5232,.T.) ;
#8984=EDGE_CURVE('',#6958,#6957,#5233,.T.) ;
#8985=EDGE_CURVE('',#6956,#6958,#5234,.T.) ;
#8986=EDGE_CURVE('',#6955,#6952,#4339,.T.) ;
#8987=EDGE_CURVE('',#6957,#6954,#4340,.T.) ;
#8988=EDGE_CURVE('',#6959,#6953,#4341,.T.) ;
#8989=EDGE_CURVE('',#6959,#6960,#5235,.T.) ;
#8990=EDGE_CURVE('',#6960,#6961,#4342,.T.) ;
#8991=EDGE_CURVE('',#6961,#6962,#5236,.T.) ;
#8992=EDGE_CURVE('',#6963,#6962,#4343,.T.) ;
#8993=EDGE_CURVE('',#6963,#6964,#5237,.T.) ;
#8994=EDGE_CURVE('',#6964,#6965,#4344,.T.) ;
#8995=EDGE_CURVE('',#6965,#6966,#5238,.T.) ;
#8996=EDGE_CURVE('',#6967,#6966,#4345,.T.) ;
#8997=EDGE_CURVE('',#6967,#6968,#5239,.T.) ;
#8998=EDGE_CURVE('',#6968,#6969,#4346,.T.) ;
#8999=EDGE_CURVE('',#6969,#6970,#5240,.T.) ;
#9000=EDGE_CURVE('',#6958,#6970,#4347,.T.) ;
#9001=EDGE_CURVE('',#6971,#6971,#4348,.F.) ;
#9002=EDGE_CURVE('',#6972,#6951,#4349,.T.) ;
#9003=EDGE_CURVE('',#6972,#6959,#5241,.T.) ;
#9004=EDGE_CURVE('',#6952,#6973,#4350,.T.) ;
#9005=EDGE_CURVE('',#6973,#6972,#85,.T.) ;
#9006=EDGE_CURVE('',#6974,#6975,#86,.T.) ;
#9007=EDGE_CURVE('',#6962,#6974,#5242,.T.) ;
#9008=EDGE_CURVE('',#6975,#6961,#5243,.T.) ;
#9009=EDGE_CURVE('',#6973,#6960,#5244,.T.) ;
#9010=EDGE_CURVE('',#6973,#6975,#4351,.T.) ;
#9011=EDGE_CURVE('',#6976,#6974,#4352,.T.) ;
#9012=EDGE_CURVE('',#6976,#6963,#5245,.T.) ;
#9013=EDGE_CURVE('',#6975,#6977,#4353,.T.) ;
#9014=EDGE_CURVE('',#6977,#6976,#87,.T.) ;
#9015=EDGE_CURVE('',#6978,#6979,#88,.T.) ;
#9016=EDGE_CURVE('',#6966,#6978,#5246,.T.) ;
#9017=EDGE_CURVE('',#6979,#6965,#5247,.T.) ;
#9018=EDGE_CURVE('',#6977,#6964,#5248,.T.) ;
#9019=EDGE_CURVE('',#6977,#6979,#4354,.T.) ;
#9020=EDGE_CURVE('',#6980,#6978,#4355,.T.) ;
#9021=EDGE_CURVE('',#6980,#6967,#5249,.T.) ;
#9022=EDGE_CURVE('',#6979,#6981,#4356,.T.) ;
#9023=EDGE_CURVE('',#6981,#6980,#89,.T.) ;
#9024=EDGE_CURVE('',#6982,#6983,#90,.T.) ;
#9025=EDGE_CURVE('',#6970,#6982,#5250,.T.) ;
#9026=EDGE_CURVE('',#6983,#6969,#5251,.T.) ;
#9027=EDGE_CURVE('',#6981,#6968,#5252,.T.) ;
#9028=EDGE_CURVE('',#6981,#6983,#4357,.T.) ;
#9029=EDGE_CURVE('',#6956,#6982,#4358,.T.) ;
#9030=EDGE_CURVE('',#6983,#6955,#4359,.T.) ;
#9031=EDGE_CURVE('',#6984,#6984,#4360,.F.) ;
#9032=EDGE_CURVE('',#6971,#6984,#5253,.T.) ;
#12848=ORIENTED_EDGE('',*,*,#8978,.F.) ;
#12849=ORIENTED_EDGE('',*,*,#8979,.F.) ;
#12850=ORIENTED_EDGE('',*,*,#8980,.F.) ;
#12851=ORIENTED_EDGE('',*,*,#8981,.F.) ;
#12852=ORIENTED_EDGE('',*,*,#8982,.F.) ;
#12853=ORIENTED_EDGE('',*,*,#8983,.T.) ;
#12854=ORIENTED_EDGE('',*,*,#8984,.F.) ;
#12855=ORIENTED_EDGE('',*,*,#8985,.F.) ;
#12856=ORIENTED_EDGE('',*,*,#8986,.T.) ;
#12857=ORIENTED_EDGE('',*,*,#8981,.T.) ;
#12858=ORIENTED_EDGE('',*,*,#8987,.F.) ;
#12859=ORIENTED_EDGE('',*,*,#8983,.F.) ;
#12860=ORIENTED_EDGE('',*,*,#8984,.T.) ;
#12861=ORIENTED_EDGE('',*,*,#8987,.T.) ;
#12862=ORIENTED_EDGE('',*,*,#8980,.T.) ;
#12863=ORIENTED_EDGE('',*,*,#8988,.F.) ;
#12864=ORIENTED_EDGE('',*,*,#8989,.T.) ;
#12865=ORIENTED_EDGE('',*,*,#8990,.T.) ;
#12866=ORIENTED_EDGE('',*,*,#8991,.T.) ;
#12867=ORIENTED_EDGE('',*,*,#8992,.F.) ;
#12868=ORIENTED_EDGE('',*,*,#8993,.T.) ;
#12869=ORIENTED_EDGE('',*,*,#8994,.T.) ;
#12870=ORIENTED_EDGE('',*,*,#8995,.T.) ;
#12871=ORIENTED_EDGE('',*,*,#8996,.F.) ;
#12872=ORIENTED_EDGE('',*,*,#8997,.T.) ;
#12873=ORIENTED_EDGE('',*,*,#8998,.T.) ;
#12874=ORIENTED_EDGE('',*,*,#8999,.T.) ;
#12875=ORIENTED_EDGE('',*,*,#9000,.F.) ;
#12876=ORIENTED_EDGE('',*,*,#9001,.F.) ;
#12877=ORIENTED_EDGE('',*,*,#8979,.T.) ;
#12878=ORIENTED_EDGE('',*,*,#9002,.F.) ;
#12879=ORIENTED_EDGE('',*,*,#9003,.T.) ;
#12880=ORIENTED_EDGE('',*,*,#8988,.T.) ;
#12881=ORIENTED_EDGE('',*,*,#8978,.T.) ;
#12882=ORIENTED_EDGE('',*,*,#9004,.T.) ;
#12883=ORIENTED_EDGE('',*,*,#9005,.T.) ;
#12884=ORIENTED_EDGE('',*,*,#9002,.T.) ;
#12885=ORIENTED_EDGE('',*,*,#9006,.F.) ;
#12886=ORIENTED_EDGE('',*,*,#9007,.F.) ;
#12887=ORIENTED_EDGE('',*,*,#8991,.F.) ;
#12888=ORIENTED_EDGE('',*,*,#9008,.F.) ;
#12889=ORIENTED_EDGE('',*,*,#9005,.F.) ;
#12890=ORIENTED_EDGE('',*,*,#9009,.T.) ;
#12891=ORIENTED_EDGE('',*,*,#8989,.F.) ;
#12892=ORIENTED_EDGE('',*,*,#9003,.F.) ;
#12893=ORIENTED_EDGE('',*,*,#9010,.T.) ;
#12894=ORIENTED_EDGE('',*,*,#9008,.T.) ;
#12895=ORIENTED_EDGE('',*,*,#8990,.F.) ;
#12896=ORIENTED_EDGE('',*,*,#9009,.F.) ;
#12897=ORIENTED_EDGE('',*,*,#9007,.T.) ;
#12898=ORIENTED_EDGE('',*,*,#9011,.F.) ;
#12899=ORIENTED_EDGE('',*,*,#9012,.T.) ;
#12900=ORIENTED_EDGE('',*,*,#8992,.T.) ;
#12901=ORIENTED_EDGE('',*,*,#9006,.T.) ;
#12902=ORIENTED_EDGE('',*,*,#9013,.T.) ;
#12903=ORIENTED_EDGE('',*,*,#9014,.T.) ;
#12904=ORIENTED_EDGE('',*,*,#9011,.T.) ;
#12905=ORIENTED_EDGE('',*,*,#9015,.F.) ;
#12906=ORIENTED_EDGE('',*,*,#9016,.F.) ;
#12907=ORIENTED_EDGE('',*,*,#8995,.F.) ;
#12908=ORIENTED_EDGE('',*,*,#9017,.F.) ;
#12909=ORIENTED_EDGE('',*,*,#9014,.F.) ;
#12910=ORIENTED_EDGE('',*,*,#9018,.T.) ;
#12911=ORIENTED_EDGE('',*,*,#8993,.F.) ;
#12912=ORIENTED_EDGE('',*,*,#9012,.F.) ;
#12913=ORIENTED_EDGE('',*,*,#9019,.T.) ;
#12914=ORIENTED_EDGE('',*,*,#9017,.T.) ;
#12915=ORIENTED_EDGE('',*,*,#8994,.F.) ;
#12916=ORIENTED_EDGE('',*,*,#9018,.F.) ;
#12917=ORIENTED_EDGE('',*,*,#9016,.T.) ;
#12918=ORIENTED_EDGE('',*,*,#9020,.F.) ;
#12919=ORIENTED_EDGE('',*,*,#9021,.T.) ;
#12920=ORIENTED_EDGE('',*,*,#8996,.T.) ;
#12921=ORIENTED_EDGE('',*,*,#9015,.T.) ;
#12922=ORIENTED_EDGE('',*,*,#9022,.T.) ;
#12923=ORIENTED_EDGE('',*,*,#9023,.T.) ;
#12924=ORIENTED_EDGE('',*,*,#9020,.T.) ;
#12925=ORIENTED_EDGE('',*,*,#9024,.F.) ;
#12926=ORIENTED_EDGE('',*,*,#9025,.F.) ;
#12927=ORIENTED_EDGE('',*,*,#8999,.F.) ;
#12928=ORIENTED_EDGE('',*,*,#9026,.F.) ;
#12929=ORIENTED_EDGE('',*,*,#9023,.F.) ;
#12930=ORIENTED_EDGE('',*,*,#9027,.T.) ;
#12931=ORIENTED_EDGE('',*,*,#8997,.F.) ;
#12932=ORIENTED_EDGE('',*,*,#9021,.F.) ;
#12933=ORIENTED_EDGE('',*,*,#9028,.T.) ;
#12934=ORIENTED_EDGE('',*,*,#9026,.T.) ;
#12935=ORIENTED_EDGE('',*,*,#8998,.F.) ;
#12936=ORIENTED_EDGE('',*,*,#9027,.F.) ;
#12937=ORIENTED_EDGE('',*,*,#8982,.T.) ;
#12938=ORIENTED_EDGE('',*,*,#9029,.T.) ;
#12939=ORIENTED_EDGE('',*,*,#9024,.T.) ;
#12940=ORIENTED_EDGE('',*,*,#9030,.T.) ;
#12941=ORIENTED_EDGE('',*,*,#8985,.T.) ;
#12942=ORIENTED_EDGE('',*,*,#9000,.T.) ;
#12943=ORIENTED_EDGE('',*,*,#9025,.T.) ;
#12944=ORIENTED_EDGE('',*,*,#9029,.F.) ;
#12945=ORIENTED_EDGE('',*,*,#9030,.F.) ;
#12946=ORIENTED_EDGE('',*,*,#9028,.F.) ;
#12947=ORIENTED_EDGE('',*,*,#9022,.F.) ;
#12948=ORIENTED_EDGE('',*,*,#9019,.F.) ;
#12949=ORIENTED_EDGE('',*,*,#9013,.F.) ;
#12950=ORIENTED_EDGE('',*,*,#9010,.F.) ;
#12951=ORIENTED_EDGE('',*,*,#9004,.F.) ;
#12952=ORIENTED_EDGE('',*,*,#8986,.F.) ;
#12953=ORIENTED_EDGE('',*,*,#9031,.T.) ;
#12954=ORIENTED_EDGE('',*,*,#9001,.T.) ;
#12955=ORIENTED_EDGE('',*,*,#9032,.T.) ;
#12956=ORIENTED_EDGE('',*,*,#9031,.F.) ;
#12957=ORIENTED_EDGE('',*,*,#9032,.F.) ;
#14563=CONICAL_SURFACE('',#17243,27.,0.785398163397448) ;
#14564=CONICAL_SURFACE('',#17251,27.,0.785398163397448) ;
#14565=CONICAL_SURFACE('',#17259,27.,0.785398163397448) ;
#14566=CONICAL_SURFACE('',#17265,27.,0.785398163397448) ;
#15307=ADVANCED_FACE('',(#2219),#1038,.F.) ;
#15308=ADVANCED_FACE('',(#2220),#1039,.F.) ;
#15309=ADVANCED_FACE('',(#2221),#1510,.T.) ;
#15310=ADVANCED_FACE('',(#2222,#757),#1040,.F.) ;
#15311=ADVANCED_FACE('',(#2223),#1511,.T.) ;
#15312=ADVANCED_FACE('',(#2224),#14563,.T.) ;
#15313=ADVANCED_FACE('',(#2225),#1041,.F.) ;
#15314=ADVANCED_FACE('',(#2226),#1042,.F.) ;
#15315=ADVANCED_FACE('',(#2227),#1512,.T.) ;
#15316=ADVANCED_FACE('',(#2228),#1513,.T.) ;
#15317=ADVANCED_FACE('',(#2229),#14564,.T.) ;
#15318=ADVANCED_FACE('',(#2230),#1043,.F.) ;
#15319=ADVANCED_FACE('',(#2231),#1044,.F.) ;
#15320=ADVANCED_FACE('',(#2232),#1514,.T.) ;
#15321=ADVANCED_FACE('',(#2233),#1515,.T.) ;
#15322=ADVANCED_FACE('',(#2234),#14565,.T.) ;
#15323=ADVANCED_FACE('',(#2235),#1045,.F.) ;
#15324=ADVANCED_FACE('',(#2236),#1046,.F.) ;
#15325=ADVANCED_FACE('',(#2237),#1516,.T.) ;
#15326=ADVANCED_FACE('',(#2238),#14566,.T.) ;
#15327=ADVANCED_FACE('',(#2239),#1517,.T.) ;
#15328=ADVANCED_FACE('',(#2240,#758),#1047,.T.) ;
#15329=ADVANCED_FACE('',(#2241),#1518,.F.) ;
#15504=CLOSED_SHELL('',(#15307,#15308,#15309,#15310,#15311,#15312,#15313,
#15314,#15315,#15316,#15317,#15318,#15319,#15320,#15321,#15322,#15323,#15324,
#15325,#15326,#15327,#15328,#15329)) ;
#17226=AXIS2_PLACEMENT_3D('',#53748,#21543,#21544) ;
#17227=AXIS2_PLACEMENT_3D('',#53749,#21545,#21546) ;
#17228=AXIS2_PLACEMENT_3D('',#53760,#21550,#21551) ;
#17229=AXIS2_PLACEMENT_3D('',#53771,#21555,#21556) ;
#17230=AXIS2_PLACEMENT_3D('',#53772,#21557,#21558) ;
#17231=AXIS2_PLACEMENT_3D('',#53773,#21559,#21560) ;
#17232=AXIS2_PLACEMENT_3D('',#53774,#21561,#21562) ;
#17233=AXIS2_PLACEMENT_3D('',#53776,#21563,#21564) ;
#17234=AXIS2_PLACEMENT_3D('',#53780,#21566,#21567) ;
#17235=AXIS2_PLACEMENT_3D('',#53784,#21569,#21570) ;
#17236=AXIS2_PLACEMENT_3D('',#53788,#21572,#21573) ;
#17237=AXIS2_PLACEMENT_3D('',#53792,#21575,#21576) ;
#17238=AXIS2_PLACEMENT_3D('',#53796,#21578,#21579) ;
#17239=AXIS2_PLACEMENT_3D('',#53799,#21581,#21582) ;
#17240=AXIS2_PLACEMENT_3D('',#53801,#21583,#21584) ;
#17241=AXIS2_PLACEMENT_3D('',#53802,#21585,#21586) ;
#17242=AXIS2_PLACEMENT_3D('',#53804,#21587,#21588) ;
#17243=AXIS2_PLACEMENT_3D('',#53806,#21590,#21591) ;
#17244=AXIS2_PLACEMENT_3D('',#53808,#21592,#21593) ;
#17245=AXIS2_PLACEMENT_3D('',#53812,#21594,#21595) ;
#17246=AXIS2_PLACEMENT_3D('',#53820,#21598,#21599) ;
#17247=AXIS2_PLACEMENT_3D('',#53822,#21601,#21602) ;
#17248=AXIS2_PLACEMENT_3D('',#53823,#21603,#21604) ;
#17249=AXIS2_PLACEMENT_3D('',#53824,#21605,#21606) ;
#17250=AXIS2_PLACEMENT_3D('',#53826,#21607,#21608) ;
#17251=AXIS2_PLACEMENT_3D('',#53828,#21610,#21611) ;
#17252=AXIS2_PLACEMENT_3D('',#53830,#21612,#21613) ;
#17253=AXIS2_PLACEMENT_3D('',#53834,#21614,#21615) ;
#17254=AXIS2_PLACEMENT_3D('',#53842,#21618,#21619) ;
#17255=AXIS2_PLACEMENT_3D('',#53844,#21621,#21622) ;
#17256=AXIS2_PLACEMENT_3D('',#53845,#21623,#21624) ;
#17257=AXIS2_PLACEMENT_3D('',#53846,#21625,#21626) ;
#17258=AXIS2_PLACEMENT_3D('',#53848,#21627,#21628) ;
#17259=AXIS2_PLACEMENT_3D('',#53850,#21630,#21631) ;
#17260=AXIS2_PLACEMENT_3D('',#53852,#21632,#21633) ;
#17261=AXIS2_PLACEMENT_3D('',#53856,#21634,#21635) ;
#17262=AXIS2_PLACEMENT_3D('',#53864,#21638,#21639) ;
#17263=AXIS2_PLACEMENT_3D('',#53866,#21641,#21642) ;
#17264=AXIS2_PLACEMENT_3D('',#53867,#21643,#21644) ;
#17265=AXIS2_PLACEMENT_3D('',#53868,#21645,#21646) ;
#17266=AXIS2_PLACEMENT_3D('',#53869,#21647,#21648) ;
#17267=AXIS2_PLACEMENT_3D('',#53870,#21649,#21650) ;
#17268=AXIS2_PLACEMENT_3D('',#53871,#21651,#21652) ;
#17269=AXIS2_PLACEMENT_3D('',#53872,#21653,#21654) ;
#17270=AXIS2_PLACEMENT_3D('',#53874,#21655,#21656) ;
#17271=AXIS2_PLACEMENT_3D('',#53875,#21657,#21658) ;
#21543=DIRECTION('axis',(0.,0.,1.)) ;
#21544=DIRECTION('refdir',(1.,0.,0.)) ;
#21545=DIRECTION('center_axis',(-1.83697019872103E-16,-1.,0.)) ;
#21546=DIRECTION('ref_axis',(-1.,1.83697019872103E-16,0.)) ;
#21547=DIRECTION('',(0.,0.,1.)) ;
#21548=DIRECTION('',(1.,-1.83697019872103E-16,0.)) ;
#21549=DIRECTION('',(0.,0.,-1.)) ;
#21550=DIRECTION('center_axis',(1.83697019872103E-16,1.,0.)) ;
#21551=DIRECTION('ref_axis',(1.,-1.83697019872103E-16,0.)) ;
#21552=DIRECTION('',(0.,0.,-1.)) ;
#21553=DIRECTION('',(-1.,1.83697019872103E-16,0.)) ;
#21554=DIRECTION('',(0.,0.,-1.)) ;
#21555=DIRECTION('center_axis',(0.,0.,-1.)) ;
#21556=DIRECTION('ref_axis',(-1.83697019872103E-16,-1.,0.)) ;
#21557=DIRECTION('center_axis',(0.,0.,-1.)) ;
#21558=DIRECTION('ref_axis',(1.,0.,0.)) ;
#21559=DIRECTION('center_axis',(0.,0.,-1.)) ;
#21560=DIRECTION('ref_axis',(-1.83697019872103E-16,-1.,0.)) ;
#21561=DIRECTION('center_axis',(0.,0.,1.)) ;
#21562=DIRECTION('ref_axis',(1.,0.,0.)) ;
#21563=DIRECTION('center_axis',(0.,0.,1.)) ;
#21564=DIRECTION('ref_axis',(1.,0.,0.)) ;
#21565=DIRECTION('',(1.22464679914735E-16,1.,0.)) ;
#21566=DIRECTION('center_axis',(0.,0.,-1.)) ;
#21567=DIRECTION('ref_axis',(-1.,1.22464679914735E-16,0.)) ;
#21568=DIRECTION('',(-1.22464679914735E-16,-1.,0.)) ;
#21569=DIRECTION('center_axis',(0.,0.,1.)) ;
#21570=DIRECTION('ref_axis',(1.,0.,0.)) ;
#21571=DIRECTION('',(1.,-6.12323399573677E-17,0.)) ;
#21572=DIRECTION('center_axis',(0.,0.,-1.)) ;
#21573=DIRECTION('ref_axis',(6.12323399573677E-17,1.,0.)) ;
#21574=DIRECTION('',(-1.,6.12323399573677E-17,0.)) ;
#21575=DIRECTION('center_axis',(0.,0.,1.)) ;
#21576=DIRECTION('ref_axis',(1.,0.,0.)) ;
#21577=DIRECTION('',(0.,-1.,0.)) ;
#21578=DIRECTION('center_axis',(0.,0.,-1.)) ;
#21579=DIRECTION('ref_axis',(1.,0.,0.)) ;
#21580=DIRECTION('',(0.,1.,0.)) ;
#21581=DIRECTION('center_axis',(0.,0.,1.)) ;
#21582=DIRECTION('ref_axis',(1.,0.,0.)) ;
#21583=DIRECTION('center_axis',(0.,0.,1.)) ;
#21584=DIRECTION('ref_axis',(1.,0.,0.)) ;
#21585=DIRECTION('center_axis',(0.,0.,1.)) ;
#21586=DIRECTION('ref_axis',(1.,0.,0.)) ;
#21587=DIRECTION('center_axis',(0.,0.,1.)) ;
#21588=DIRECTION('ref_axis',(1.,0.,0.)) ;
#21589=DIRECTION('',(0.,0.,-1.)) ;
#21590=DIRECTION('center_axis',(0.,0.,-1.)) ;
#21591=DIRECTION('ref_axis',(1.,0.,0.)) ;
#21592=DIRECTION('center_axis',(0.,0.,-1.)) ;
#21593=DIRECTION('ref_axis',(1.,0.,0.)) ;
#21594=DIRECTION('center_axis',(-1.,1.22464679914735E-16,0.)) ;
#21595=DIRECTION('ref_axis',(1.22464679914735E-16,1.,0.)) ;
#21596=DIRECTION('',(0.,0.,1.)) ;
#21597=DIRECTION('',(0.,0.,-1.)) ;
#21598=DIRECTION('center_axis',(1.,-1.22464679914735E-16,0.)) ;
#21599=DIRECTION('ref_axis',(-1.22464679914735E-16,-1.,0.)) ;
#21600=DIRECTION('',(0.,0.,-1.)) ;
#21601=DIRECTION('center_axis',(0.,0.,-1.)) ;
#21602=DIRECTION('ref_axis',(-1.,1.22464679914735E-16,0.)) ;
#21603=DIRECTION('center_axis',(0.,0.,-1.)) ;
#21604=DIRECTION('ref_axis',(1.,0.,0.)) ;
#21605=DIRECTION('center_axis',(0.,0.,1.)) ;
#21606=DIRECTION('ref_axis',(1.,0.,0.)) ;
#21607=DIRECTION('center_axis',(0.,0.,1.)) ;
#21608=DIRECTION('ref_axis',(1.,0.,0.)) ;
#21609=DIRECTION('',(0.,0.,-1.)) ;
#21610=DIRECTION('center_axis',(0.,0.,-1.)) ;
#21611=DIRECTION('ref_axis',(1.,0.,0.)) ;
#21612=DIRECTION('center_axis',(0.,0.,-1.)) ;
#21613=DIRECTION('ref_axis',(1.,0.,0.)) ;
#21614=DIRECTION('center_axis',(6.12323399573677E-17,1.,0.)) ;
#21615=DIRECTION('ref_axis',(1.,-6.12323399573677E-17,0.)) ;
#21616=DIRECTION('',(0.,0.,1.)) ;
#21617=DIRECTION('',(0.,0.,-1.)) ;
#21618=DIRECTION('center_axis',(-6.12323399573677E-17,-1.,0.)) ;
#21619=DIRECTION('ref_axis',(-1.,6.12323399573677E-17,0.)) ;
#21620=DIRECTION('',(0.,0.,-1.)) ;
#21621=DIRECTION('center_axis',(0.,0.,-1.)) ;
#21622=DIRECTION('ref_axis',(6.12323399573677E-17,1.,0.)) ;
#21623=DIRECTION('center_axis',(0.,0.,-1.)) ;
#21624=DIRECTION('ref_axis',(1.,0.,0.)) ;
#21625=DIRECTION('center_axis',(0.,0.,1.)) ;
#21626=DIRECTION('ref_axis',(1.,0.,0.)) ;
#21627=DIRECTION('center_axis',(0.,0.,1.)) ;
#21628=DIRECTION('ref_axis',(1.,0.,0.)) ;
#21629=DIRECTION('',(0.,0.,-1.)) ;
#21630=DIRECTION('center_axis',(0.,0.,-1.)) ;
#21631=DIRECTION('ref_axis',(1.,0.,0.)) ;
#21632=DIRECTION('center_axis',(0.,0.,-1.)) ;
#21633=DIRECTION('ref_axis',(1.,0.,0.)) ;
#21634=DIRECTION('center_axis',(1.,0.,0.)) ;
#21635=DIRECTION('ref_axis',(0.,-1.,0.)) ;
#21636=DIRECTION('',(0.,0.,1.)) ;
#21637=DIRECTION('',(0.,0.,-1.)) ;
#21638=DIRECTION('center_axis',(-1.,0.,0.)) ;
#21639=DIRECTION('ref_axis',(0.,1.,0.)) ;
#21640=DIRECTION('',(0.,0.,-1.)) ;
#21641=DIRECTION('center_axis',(0.,0.,-1.)) ;
#21642=DIRECTION('ref_axis',(1.,0.,0.)) ;
#21643=DIRECTION('center_axis',(0.,0.,-1.)) ;
#21644=DIRECTION('ref_axis',(1.,0.,0.)) ;
#21645=DIRECTION('center_axis',(0.,0.,-1.)) ;
#21646=DIRECTION('ref_axis',(1.,0.,0.)) ;
#21647=DIRECTION('center_axis',(0.,0.,1.)) ;
#21648=DIRECTION('ref_axis',(1.,0.,0.)) ;
#21649=DIRECTION('center_axis',(0.,0.,-1.)) ;
#21650=DIRECTION('ref_axis',(1.,0.,0.)) ;
#21651=DIRECTION('center_axis',(0.,0.,1.)) ;
#21652=DIRECTION('ref_axis',(1.,0.,0.)) ;
#21653=DIRECTION('center_axis',(0.,0.,1.)) ;
#21654=DIRECTION('ref_axis',(1.,0.,0.)) ;
#21655=DIRECTION('center_axis',(0.,0.,1.)) ;
#21656=DIRECTION('ref_axis',(1.,0.,0.)) ;
#21657=DIRECTION('center_axis',(0.,0.,1.)) ;
#21658=DIRECTION('ref_axis',(1.,0.,0.)) ;
#21659=DIRECTION('',(0.,0.,1.)) ;
#53748=CARTESIAN_POINT('',(0.,0.,0.)) ;
#53749=CARTESIAN_POINT('Origin',(28.8444102037119,-3.00000000000001,10.)) ;
#53750=CARTESIAN_POINT('',(28.8444102037119,-3.00000000000001,6.)) ;
#53751=CARTESIAN_POINT('',(24.8193472919817,-3.,10.)) ;
#53752=CARTESIAN_POINT('Ctrl Pts',(28.8444102037119,-3.00000000000001,6.)) ;
#53753=CARTESIAN_POINT('Ctrl Pts',(26.6828023435557,-3.00000000000001,8.1500104764796)) ;
#53754=CARTESIAN_POINT('Ctrl Pts',(24.8193472919817,-3.00000000000001,10.)) ;
#53755=CARTESIAN_POINT('',(28.8444102037119,-3.00000000000001,0.)) ;
#53756=CARTESIAN_POINT('',(28.8444102037119,-3.00000000000001,0.)) ;
#53757=CARTESIAN_POINT('',(24.8193472919817,-3.,0.)) ;
#53758=CARTESIAN_POINT('',(14.422205101856,-3.,0.)) ;
#53759=CARTESIAN_POINT('',(24.8193472919817,-3.,10.)) ;
#53760=CARTESIAN_POINT('Origin',(24.8193472919817,3.,10.)) ;
#53761=CARTESIAN_POINT('',(24.8193472919817,3.,10.)) ;
#53762=CARTESIAN_POINT('',(28.8444102037119,2.99999999999999,6.)) ;
#53763=CARTESIAN_POINT('Ctrl Pts',(24.8193472919817,3.,10.)) ;
#53764=CARTESIAN_POINT('Ctrl Pts',(26.6828023431939,3.,8.15001047683915)) ;
#53765=CARTESIAN_POINT('Ctrl Pts',(28.8444102037119,2.99999999999999,6.)) ;
#53766=CARTESIAN_POINT('',(24.8193472919817,3.,0.)) ;
#53767=CARTESIAN_POINT('',(24.8193472919817,3.,10.)) ;
#53768=CARTESIAN_POINT('',(28.8444102037119,2.99999999999999,0.)) ;
#53769=CARTESIAN_POINT('',(12.4096736459909,3.,0.)) ;
#53770=CARTESIAN_POINT('',(28.8444102037119,2.99999999999999,0.)) ;
#53771=CARTESIAN_POINT('Origin',(0.,0.,10.)) ;
#53772=CARTESIAN_POINT('Origin',(0.,0.,10.)) ;
#53773=CARTESIAN_POINT('Origin',(0.,0.,0.)) ;
#53774=CARTESIAN_POINT('Origin',(0.,0.,0.)) ;
#53775=CARTESIAN_POINT('',(3.,-28.8444102037119,0.)) ;
#53776=CARTESIAN_POINT('Origin',(0.,0.,0.)) ;
#53777=CARTESIAN_POINT('',(3.,-24.8193472919817,0.)) ;
#53778=CARTESIAN_POINT('',(3.,-12.4096736459909,0.)) ;
#53779=CARTESIAN_POINT('',(-3.,-24.8193472919817,0.)) ;
#53780=CARTESIAN_POINT('Origin',(0.,0.,0.)) ;
#53781=CARTESIAN_POINT('',(-3.,-28.8444102037119,0.)) ;
#53782=CARTESIAN_POINT('',(-3.,-14.422205101856,0.)) ;
#53783=CARTESIAN_POINT('',(-28.8444102037119,-3.,0.)) ;
#53784=CARTESIAN_POINT('Origin',(0.,0.,0.)) ;
#53785=CARTESIAN_POINT('',(-24.8193472919817,-3.,0.)) ;
#53786=CARTESIAN_POINT('',(-12.4096736459909,-3.,0.)) ;
#53787=CARTESIAN_POINT('',(-24.8193472919817,3.,0.)) ;
#53788=CARTESIAN_POINT('Origin',(0.,0.,0.)) ;
#53789=CARTESIAN_POINT('',(-28.8444102037119,3.,0.)) ;
#53790=CARTESIAN_POINT('',(-14.422205101856,3.,0.)) ;
#53791=CARTESIAN_POINT('',(-3.,28.8444102037119,0.)) ;
#53792=CARTESIAN_POINT('Origin',(0.,0.,0.)) ;
#53793=CARTESIAN_POINT('',(-3.,24.8193472919817,0.)) ;
#53794=CARTESIAN_POINT('',(-3.,12.4096736459909,0.)) ;
#53795=CARTESIAN_POINT('',(3.,24.8193472919817,0.)) ;
#53796=CARTESIAN_POINT('Origin',(0.,0.,0.)) ;
#53797=CARTESIAN_POINT('',(3.,28.8444102037119,0.)) ;
#53798=CARTESIAN_POINT('',(3.,14.422205101856,0.)) ;
#53799=CARTESIAN_POINT('Origin',(0.,0.,0.)) ;
#53800=CARTESIAN_POINT('',(-18.7631,-2.29781703570817E-15,0.)) ;
#53801=CARTESIAN_POINT('Origin',(0.,0.,0.)) ;
#53802=CARTESIAN_POINT('Origin',(0.,0.,0.)) ;
#53803=CARTESIAN_POINT('',(3.,-28.8444102037119,6.)) ;
#53804=CARTESIAN_POINT('Origin',(0.,0.,6.)) ;
#53805=CARTESIAN_POINT('',(3.,-28.8444102037119,0.)) ;
#53806=CARTESIAN_POINT('Origin',(0.,0.,8.)) ;
#53807=CARTESIAN_POINT('',(3.,-24.8193472919817,10.)) ;
#53808=CARTESIAN_POINT('Origin',(0.,0.,10.)) ;
#53809=CARTESIAN_POINT('Ctrl Pts',(3.,-24.8193472919817,10.)) ;
#53810=CARTESIAN_POINT('Ctrl Pts',(3.,-26.6828023431939,8.15001047683915)) ;
#53811=CARTESIAN_POINT('Ctrl Pts',(3.,-28.8444102037119,6.)) ;
#53812=CARTESIAN_POINT('Origin',(-3.,-28.8444102037119,10.)) ;
#53813=CARTESIAN_POINT('',(-3.,-28.8444102037119,6.)) ;
#53814=CARTESIAN_POINT('',(-3.,-24.8193472919817,10.)) ;
#53815=CARTESIAN_POINT('Ctrl Pts',(-3.,-28.8444102037119,6.)) ;
#53816=CARTESIAN_POINT('Ctrl Pts',(-3.,-26.6828023431939,8.15001047683915)) ;
#53817=CARTESIAN_POINT('Ctrl Pts',(-3.,-24.8193472919817,10.)) ;
#53818=CARTESIAN_POINT('',(-3.,-28.8444102037119,0.)) ;
#53819=CARTESIAN_POINT('',(-3.,-24.8193472919817,10.)) ;
#53820=CARTESIAN_POINT('Origin',(3.,-24.8193472919817,10.)) ;
#53821=CARTESIAN_POINT('',(3.,-24.8193472919817,10.)) ;
#53822=CARTESIAN_POINT('Origin',(0.,0.,10.)) ;
#53823=CARTESIAN_POINT('Origin',(0.,0.,10.)) ;
#53824=CARTESIAN_POINT('Origin',(0.,0.,0.)) ;
#53825=CARTESIAN_POINT('',(-28.8444102037119,-3.,6.)) ;
#53826=CARTESIAN_POINT('Origin',(0.,0.,6.)) ;
#53827=CARTESIAN_POINT('',(-28.8444102037119,-3.,0.)) ;
#53828=CARTESIAN_POINT('Origin',(0.,0.,8.)) ;
#53829=CARTESIAN_POINT('',(-24.8193472919817,-3.,10.)) ;
#53830=CARTESIAN_POINT('Origin',(0.,0.,10.)) ;
#53831=CARTESIAN_POINT('Ctrl Pts',(-24.8193472919817,-3.,10.)) ;
#53832=CARTESIAN_POINT('Ctrl Pts',(-26.6828023431939,-3.,8.15001047683915)) ;
#53833=CARTESIAN_POINT('Ctrl Pts',(-28.8444102037119,-3.,6.)) ;
#53834=CARTESIAN_POINT('Origin',(-28.8444102037119,3.,10.)) ;
#53835=CARTESIAN_POINT('',(-28.8444102037119,3.,6.)) ;
#53836=CARTESIAN_POINT('',(-24.8193472919817,3.,10.)) ;
#53837=CARTESIAN_POINT('Ctrl Pts',(-28.8444102037119,3.,6.)) ;
#53838=CARTESIAN_POINT('Ctrl Pts',(-26.6828023431939,3.,8.15001047683915)) ;
#53839=CARTESIAN_POINT('Ctrl Pts',(-24.8193472919817,3.,10.)) ;
#53840=CARTESIAN_POINT('',(-28.8444102037119,3.,0.)) ;
#53841=CARTESIAN_POINT('',(-24.8193472919817,3.,10.)) ;
#53842=CARTESIAN_POINT('Origin',(-24.8193472919817,-3.,10.)) ;
#53843=CARTESIAN_POINT('',(-24.8193472919817,-3.,10.)) ;
#53844=CARTESIAN_POINT('Origin',(0.,0.,10.)) ;
#53845=CARTESIAN_POINT('Origin',(0.,0.,10.)) ;
#53846=CARTESIAN_POINT('Origin',(0.,0.,0.)) ;
#53847=CARTESIAN_POINT('',(-3.,28.8444102037119,6.)) ;
#53848=CARTESIAN_POINT('Origin',(0.,0.,6.)) ;
#53849=CARTESIAN_POINT('',(-3.,28.8444102037119,0.)) ;
#53850=CARTESIAN_POINT('Origin',(0.,0.,8.)) ;
#53851=CARTESIAN_POINT('',(-3.,24.8193472919817,10.)) ;
#53852=CARTESIAN_POINT('Origin',(0.,0.,10.)) ;
#53853=CARTESIAN_POINT('Ctrl Pts',(-3.,24.8193472919817,10.)) ;
#53854=CARTESIAN_POINT('Ctrl Pts',(-3.,26.6828023431935,8.15001047683959)) ;
#53855=CARTESIAN_POINT('Ctrl Pts',(-3.,28.8444102037119,6.)) ;
#53856=CARTESIAN_POINT('Origin',(3.,28.8444102037119,10.)) ;
#53857=CARTESIAN_POINT('',(3.,28.8444102037119,6.)) ;
#53858=CARTESIAN_POINT('',(3.,24.8193472919817,10.)) ;
#53859=CARTESIAN_POINT('Ctrl Pts',(3.,28.8444102037119,6.)) ;
#53860=CARTESIAN_POINT('Ctrl Pts',(3.,26.6828023431935,8.15001047683959)) ;
#53861=CARTESIAN_POINT('Ctrl Pts',(3.,24.8193472919817,10.)) ;
#53862=CARTESIAN_POINT('',(3.,28.8444102037119,0.)) ;
#53863=CARTESIAN_POINT('',(3.,24.8193472919817,10.)) ;
#53864=CARTESIAN_POINT('Origin',(-3.,24.8193472919817,10.)) ;
#53865=CARTESIAN_POINT('',(-3.,24.8193472919817,10.)) ;
#53866=CARTESIAN_POINT('Origin',(0.,0.,10.)) ;
#53867=CARTESIAN_POINT('Origin',(0.,0.,10.)) ;
#53868=CARTESIAN_POINT('Origin',(0.,0.,8.)) ;
#53869=CARTESIAN_POINT('Origin',(0.,0.,6.)) ;
#53870=CARTESIAN_POINT('Origin',(0.,0.,10.)) ;
#53871=CARTESIAN_POINT('Origin',(0.,0.,0.)) ;
#53872=CARTESIAN_POINT('Origin',(0.,0.,10.)) ;
#53873=CARTESIAN_POINT('',(-18.7631,-2.29781703570817E-15,10.)) ;
#53874=CARTESIAN_POINT('Origin',(0.,0.,10.)) ;
#53875=CARTESIAN_POINT('Origin',(0.,0.,0.)) ;
#53876=CARTESIAN_POINT('',(-18.7631,-2.29781703570817E-15,0.)) ;
#63802=UNCERTAINTY_MEASURE_WITH_UNIT(LENGTH_MEASURE(0.01),#63825,
'DISTANCE_ACCURACY_VALUE',
'Maximum model space distance between geometric entities at asserted c
onnectivities') ;
#63807=UNCERTAINTY_MEASURE_WITH_UNIT(LENGTH_MEASURE(0.01),#63825,
'DISTANCE_ACCURACY_VALUE',
'Maximum model space distance between geometric entities at asserted c
onnectivities') ;
#63819=(
GEOMETRIC_REPRESENTATION_CONTEXT(3)
GLOBAL_UNCERTAINTY_ASSIGNED_CONTEXT((#63802))
GLOBAL_UNIT_ASSIGNED_CONTEXT((#63825,#63827,#63828))
REPRESENTATION_CONTEXT('','3D')
) ;
#63824=(
GEOMETRIC_REPRESENTATION_CONTEXT(3)
GLOBAL_UNCERTAINTY_ASSIGNED_CONTEXT((#63807))
GLOBAL_UNIT_ASSIGNED_CONTEXT((#63825,#63827,#63828))
REPRESENTATION_CONTEXT('','3D')
) ;
#63825=(
LENGTH_UNIT()
NAMED_UNIT(*)
SI_UNIT(.MILLI.,.METRE.)
) ;
#63827=(
NAMED_UNIT(*)
PLANE_ANGLE_UNIT()
SI_UNIT($,.RADIAN.)
) ;
#63828=(
NAMED_UNIT(*)
SI_UNIT($,.STERADIAN.)
SOLID_ANGLE_UNIT()
) ;
#63840=SHAPE_DEFINITION_REPRESENTATION(#63856,#63889) ;
#63856=PRODUCT_DEFINITION_SHAPE('',$,#63906) ;
#63889=SHAPE_REPRESENTATION('',(#17226),#63819) ;
#63894=PRODUCT_DEFINITION_CONTEXT('part definition',#63944,'design') ;
#63906=PRODUCT_DEFINITION('Bearing_Lock_Nut','Bearing_Lock_Nut',#63922,
#63894) ;
#63922=PRODUCT_DEFINITION_FORMATION('',$,#63957) ;
#63944=APPLICATION_CONTEXT(
'Core Data for Automotive Mechanical Design Process') ;
#63945=PRODUCT_CONTEXT('part definition',#63944,'mechanical') ;
#63957=PRODUCT('Bearing_Lock_Nut','Bearing_Lock_Nut',$,(#63945)) ;
#63966=PRESENTATION_STYLE_ASSIGNMENT((#63971)) ;
#63971=SURFACE_STYLE_USAGE(.BOTH.,#63976) ;
#63976=SURFACE_SIDE_STYLE('',(#63981)) ;
#63981=SURFACE_STYLE_FILL_AREA(#63986) ;
#63986=FILL_AREA_STYLE('Opaque(115,115,115)',(#63991)) ;
#63991=FILL_AREA_STYLE_COLOUR('Opaque(115,115,115)',#63996) ;
#63996=COLOUR_RGB('Opaque(115,115,115)', 0.72549020, 0.75294118, 0.79215686) ;
ENDSEC;
END-ISO-10303-21;
